ISO-10303-21;
HEADER;
/* Generated by software containing ST-Developer
 * from STEP Tools, Inc. (www.steptools.com) 
 */

FILE_DESCRIPTION(
/* description */ (''),
/* implementation_level */ '2;1');

FILE_NAME(
/* name */ 'Bearing_02.step',
/* time_stamp */ '2026-10-19T01:30:23+06:00',
/* author */ (''),
/* organization */ (''),
/* preprocessor_version */ 'ST-DEVELOPER v20.2',
/* originating_system */ 'Autodesk Translation Framework v15.15.0.0',
/* authorisation */ '');

FILE_SCHEMA (('AUTOMOTIVE_DESIGN { 1 0 10303 214 3 1 1 }'));
ENDSEC;

DATA;
#10=MECHANICAL_DESIGN_GEOMETRIC_PRESENTATION_REPRESENTATION('',(#92),#10639);
#72=SHAPE_REPRESENTATION_RELATIONSHIP('SRR','None',#10682,#82);
#82=ADVANCED_BREP_SHAPE_REPRESENTATION('',(#102),#10634);
#92=STYLED_ITEM('',(#10790),#102);
#102=MANIFOLD_SOLID_BREP('Bearing_02',#5718);
#227=TOROIDAL_SURFACE('',#6428,4.3,0.3);
#228=TOROIDAL_SURFACE('',#6438,4.7,0.3);
#229=TOROIDAL_SURFACE('',#6445,4.3,0.3);
#230=TOROIDAL_SURFACE('',#6450,4.7,0.3);
#282=FACE_BOUND('',#1078,.T.);
#283=FACE_BOUND('',#1084,.T.);
#359=PLANE('',#6433);
#360=PLANE('',#6448);
#654=FACE_OUTER_BOUND('',#1076,.T.);
#655=FACE_OUTER_BOUND('',#1077,.T.);
#656=FACE_OUTER_BOUND('',#1079,.T.);
#657=FACE_OUTER_BOUND('',#1080,.T.);
#658=FACE_OUTER_BOUND('',#1081,.T.);
#659=FACE_OUTER_BOUND('',#1082,.T.);
#660=FACE_OUTER_BOUND('',#1083,.T.);
#661=FACE_OUTER_BOUND('',#1085,.T.);
#1076=EDGE_LOOP('',(#4672,#4673,#4674,#4675,#4676));
#1077=EDGE_LOOP('',(#4677));
#1078=EDGE_LOOP('',(#4678));
#1079=EDGE_LOOP('',(#4679,#4680,#4681,#4682,#4683,#4684));
#1080=EDGE_LOOP('',(#4685,#4686,#4687,#4688,#4689));
#1081=EDGE_LOOP('',(#4690,#4691,#4692,#4693,#4694,#4695));
#1082=EDGE_LOOP('',(#4696,#4697,#4698,#4699,#4700));
#1083=EDGE_LOOP('',(#4701));
#1084=EDGE_LOOP('',(#4702));
#1085=EDGE_LOOP('',(#4703,#4704,#4705,#4706,#4707));
#1440=LINE('',#10021,#1770);
#1441=LINE('',#10033,#1771);
#1770=VECTOR('',#8136,4.);
#1771=VECTOR('',#8151,5.);
#2164=CIRCLE('',#6429,4.3);
#2165=CIRCLE('',#6430,0.3);
#2166=CIRCLE('',#6431,4.);
#2167=CIRCLE('',#6432,4.);
#2168=CIRCLE('',#6434,4.7);
#2169=CIRCLE('',#6436,4.);
#2170=CIRCLE('',#6437,4.);
#2171=CIRCLE('',#6439,0.3);
#2172=CIRCLE('',#6440,5.);
#2173=CIRCLE('',#6441,5.);
#2174=CIRCLE('',#6443,5.);
#2175=CIRCLE('',#6444,5.);
#2176=CIRCLE('',#6446,4.3);
#2177=CIRCLE('',#6447,0.3);
#2178=CIRCLE('',#6449,4.7);
#2179=CIRCLE('',#6451,0.3);
#2618=VERTEX_POINT('',#10009);
#2619=VERTEX_POINT('',#10011);
#2620=VERTEX_POINT('',#10013);
#2621=VERTEX_POINT('',#10017);
#2622=VERTEX_POINT('',#10020);
#2623=VERTEX_POINT('',#10022);
#2624=VERTEX_POINT('',#10026);
#2625=VERTEX_POINT('',#10028);
#2626=VERTEX_POINT('',#10032);
#2627=VERTEX_POINT('',#10034);
#2628=VERTEX_POINT('',#10038);
#2629=VERTEX_POINT('',#10042);
#3312=EDGE_CURVE('',#2618,#2618,#2164,.T.);
#3313=EDGE_CURVE('',#2618,#2619,#2165,.T.);
#3314=EDGE_CURVE('',#2620,#2619,#2166,.T.);
#3315=EDGE_CURVE('',#2619,#2620,#2167,.T.);
#3316=EDGE_CURVE('',#2621,#2621,#2168,.T.);
#3317=EDGE_CURVE('',#2620,#2622,#1440,.T.);
#3318=EDGE_CURVE('',#2622,#2623,#2169,.T.);
#3319=EDGE_CURVE('',#2623,#2622,#2170,.T.);
#3320=EDGE_CURVE('',#2621,#2624,#2171,.T.);
#3321=EDGE_CURVE('',#2625,#2624,#2172,.T.);
#3322=EDGE_CURVE('',#2624,#2625,#2173,.T.);
#3323=EDGE_CURVE('',#2625,#2626,#1441,.T.);
#3324=EDGE_CURVE('',#2626,#2627,#2174,.T.);
#3325=EDGE_CURVE('',#2627,#2626,#2175,.T.);
#3326=EDGE_CURVE('',#2628,#2628,#2176,.T.);
#3327=EDGE_CURVE('',#2628,#2623,#2177,.T.);
#3328=EDGE_CURVE('',#2629,#2629,#2178,.T.);
#3329=EDGE_CURVE('',#2629,#2627,#2179,.T.);
#4672=ORIENTED_EDGE('',*,*,#3312,.F.);
#4673=ORIENTED_EDGE('',*,*,#3313,.T.);
#4674=ORIENTED_EDGE('',*,*,#3314,.F.);
#4675=ORIENTED_EDGE('',*,*,#3315,.F.);
#4676=ORIENTED_EDGE('',*,*,#3313,.F.);
#4677=ORIENTED_EDGE('',*,*,#3316,.T.);
#4678=ORIENTED_EDGE('',*,*,#3312,.T.);
#4679=ORIENTED_EDGE('',*,*,#3314,.T.);
#4680=ORIENTED_EDGE('',*,*,#3315,.T.);
#4681=ORIENTED_EDGE('',*,*,#3317,.T.);
#4682=ORIENTED_EDGE('',*,*,#3318,.T.);
#4683=ORIENTED_EDGE('',*,*,#3319,.T.);
#4684=ORIENTED_EDGE('',*,*,#3317,.F.);
#4685=ORIENTED_EDGE('',*,*,#3316,.F.);
#4686=ORIENTED_EDGE('',*,*,#3320,.T.);
#4687=ORIENTED_EDGE('',*,*,#3321,.F.);
#4688=ORIENTED_EDGE('',*,*,#3322,.F.);
#4689=ORIENTED_EDGE('',*,*,#3320,.F.);
#4690=ORIENTED_EDGE('',*,*,#3321,.T.);
#4691=ORIENTED_EDGE('',*,*,#3322,.T.);
#4692=ORIENTED_EDGE('',*,*,#3323,.T.);
#4693=ORIENTED_EDGE('',*,*,#3324,.T.);
#4694=ORIENTED_EDGE('',*,*,#3325,.T.);
#4695=ORIENTED_EDGE('',*,*,#3323,.F.);
#4696=ORIENTED_EDGE('',*,*,#3326,.F.);
#4697=ORIENTED_EDGE('',*,*,#3327,.T.);
#4698=ORIENTED_EDGE('',*,*,#3318,.F.);
#4699=ORIENTED_EDGE('',*,*,#3319,.F.);
#4700=ORIENTED_EDGE('',*,*,#3327,.F.);
#4701=ORIENTED_EDGE('',*,*,#3328,.T.);
#4702=ORIENTED_EDGE('',*,*,#3326,.T.);
#4703=ORIENTED_EDGE('',*,*,#3328,.F.);
#4704=ORIENTED_EDGE('',*,*,#3329,.T.);
#4705=ORIENTED_EDGE('',*,*,#3324,.F.);
#4706=ORIENTED_EDGE('',*,*,#3325,.F.);
#4707=ORIENTED_EDGE('',*,*,#3329,.F.);
#5274=CYLINDRICAL_SURFACE('',#6435,4.);
#5275=CYLINDRICAL_SURFACE('',#6442,5.);
#5597=ADVANCED_FACE('',(#654),#227,.T.);
#5598=ADVANCED_FACE('',(#655,#282),#359,.T.);
#5599=ADVANCED_FACE('',(#656),#5274,.F.);
#5600=ADVANCED_FACE('',(#657),#228,.T.);
#5601=ADVANCED_FACE('',(#658),#5275,.T.);
#5602=ADVANCED_FACE('',(#659),#229,.T.);
#5603=ADVANCED_FACE('',(#660,#283),#360,.F.);
#5604=ADVANCED_FACE('',(#661),#230,.T.);
#5718=CLOSED_SHELL('',(#5597,#5598,#5599,#5600,#5601,#5602,#5603,#5604));
#6427=AXIS2_PLACEMENT_3D('',#10007,#8118,#8119);
#6428=AXIS2_PLACEMENT_3D('',#10008,#8120,#8121);
#6429=AXIS2_PLACEMENT_3D('',#10010,#8122,#8123);
#6430=AXIS2_PLACEMENT_3D('',#10012,#8124,#8125);
#6431=AXIS2_PLACEMENT_3D('',#10014,#8126,#8127);
#6432=AXIS2_PLACEMENT_3D('',#10015,#8128,#8129);
#6433=AXIS2_PLACEMENT_3D('',#10016,#8130,#8131);
#6434=AXIS2_PLACEMENT_3D('',#10018,#8132,#8133);
#6435=AXIS2_PLACEMENT_3D('',#10019,#8134,#8135);
#6436=AXIS2_PLACEMENT_3D('',#10023,#8137,#8138);
#6437=AXIS2_PLACEMENT_3D('',#10024,#8139,#8140);
#6438=AXIS2_PLACEMENT_3D('',#10025,#8141,#8142);
#6439=AXIS2_PLACEMENT_3D('',#10027,#8143,#8144);
#6440=AXIS2_PLACEMENT_3D('',#10029,#8145,#8146);
#6441=AXIS2_PLACEMENT_3D('',#10030,#8147,#8148);
#6442=AXIS2_PLACEMENT_3D('',#10031,#8149,#8150);
#6443=AXIS2_PLACEMENT_3D('',#10035,#8152,#8153);
#6444=AXIS2_PLACEMENT_3D('',#10036,#8154,#8155);
#6445=AXIS2_PLACEMENT_3D('',#10037,#8156,#8157);
#6446=AXIS2_PLACEMENT_3D('',#10039,#8158,#8159);
#6447=AXIS2_PLACEMENT_3D('',#10040,#8160,#8161);
#6448=AXIS2_PLACEMENT_3D('',#10041,#8162,#8163);
#6449=AXIS2_PLACEMENT_3D('',#10043,#8164,#8165);
#6450=AXIS2_PLACEMENT_3D('',#10044,#8166,#8167);
#6451=AXIS2_PLACEMENT_3D('',#10045,#8168,#8169);
#8118=DIRECTION('axis',(0.,0.,1.));
#8119=DIRECTION('refdir',(1.,0.,0.));
#8120=DIRECTION('center_axis',(1.,0.,0.));
#8121=DIRECTION('ref_axis',(0.,0.,1.));
#8122=DIRECTION('center_axis',(1.,0.,0.));
#8123=DIRECTION('ref_axis',(0.,-1.,0.));
#8124=DIRECTION('center_axis',(0.,1.,0.));
#8125=DIRECTION('ref_axis',(0.,0.,-1.));
#8126=DIRECTION('center_axis',(-1.,0.,0.));
#8127=DIRECTION('ref_axis',(0.,-1.,0.));
#8128=DIRECTION('center_axis',(-1.,0.,0.));
#8129=DIRECTION('ref_axis',(0.,-1.,0.));
#8130=DIRECTION('center_axis',(-1.,0.,0.));
#8131=DIRECTION('ref_axis',(0.,-1.,0.));
#8132=DIRECTION('center_axis',(-1.,0.,0.));
#8133=DIRECTION('ref_axis',(0.,-1.,0.));
#8134=DIRECTION('center_axis',(1.,0.,0.));
#8135=DIRECTION('ref_axis',(0.,-1.,0.));
#8136=DIRECTION('',(1.,0.,0.));
#8137=DIRECTION('center_axis',(1.,0.,0.));
#8138=DIRECTION('ref_axis',(0.,-1.,0.));
#8139=DIRECTION('center_axis',(1.,0.,0.));
#8140=DIRECTION('ref_axis',(0.,-1.,0.));
#8141=DIRECTION('center_axis',(-1.,0.,0.));
#8142=DIRECTION('ref_axis',(0.,0.,-1.));
#8143=DIRECTION('center_axis',(0.,1.,0.));
#8144=DIRECTION('ref_axis',(0.,0.,1.));
#8145=DIRECTION('center_axis',(1.,0.,0.));
#8146=DIRECTION('ref_axis',(0.,-1.,0.));
#8147=DIRECTION('center_axis',(1.,0.,0.));
#8148=DIRECTION('ref_axis',(0.,-1.,0.));
#8149=DIRECTION('center_axis',(1.,0.,0.));
#8150=DIRECTION('ref_axis',(0.,-1.,0.));
#8151=DIRECTION('',(1.,0.,0.));
#8152=DIRECTION('center_axis',(-1.,0.,0.));
#8153=DIRECTION('ref_axis',(0.,-1.,0.));
#8154=DIRECTION('center_axis',(-1.,0.,0.));
#8155=DIRECTION('ref_axis',(0.,-1.,0.));
#8156=DIRECTION('center_axis',(-1.,0.,0.));
#8157=DIRECTION('ref_axis',(0.,0.,-1.));
#8158=DIRECTION('center_axis',(-1.,0.,0.));
#8159=DIRECTION('ref_axis',(0.,-1.,0.));
#8160=DIRECTION('center_axis',(0.,1.,0.));
#8161=DIRECTION('ref_axis',(0.,0.,1.));
#8162=DIRECTION('center_axis',(-1.,0.,0.));
#8163=DIRECTION('ref_axis',(0.,-1.,0.));
#8164=DIRECTION('center_axis',(1.,0.,0.));
#8165=DIRECTION('ref_axis',(0.,-1.,0.));
#8166=DIRECTION('center_axis',(1.,0.,0.));
#8167=DIRECTION('ref_axis',(0.,0.,1.));
#8168=DIRECTION('center_axis',(0.,1.,0.));
#8169=DIRECTION('ref_axis',(0.,0.,-1.));
#10007=CARTESIAN_POINT('',(0.,0.,0.));
#10008=CARTESIAN_POINT('Origin',(13.3,21.9999999999999,-1.92966607280848));
#10009=CARTESIAN_POINT('',(13.,21.9999999999999,-6.22966607280848));
#10010=CARTESIAN_POINT('Origin',(13.,21.9999999999999,-1.92966607280848));
#10011=CARTESIAN_POINT('',(13.3,21.9999999999999,-5.92966607280848));
#10012=CARTESIAN_POINT('Origin',(13.3,21.9999999999999,-6.22966607280848));
#10013=CARTESIAN_POINT('',(13.3,25.9999999999999,-1.92966607280848));
#10014=CARTESIAN_POINT('Origin',(13.3,21.9999999999999,-1.92966607280848));
#10015=CARTESIAN_POINT('Origin',(13.3,21.9999999999999,-1.92966607280848));
#10016=CARTESIAN_POINT('Origin',(13.,21.9999999999999,-1.92966607280848));
#10017=CARTESIAN_POINT('',(13.,21.9999999999999,2.77033392719152));
#10018=CARTESIAN_POINT('Origin',(13.,21.9999999999999,-1.92966607280848));
#10019=CARTESIAN_POINT('Origin',(29.,21.9999999999999,-1.92966607280848));
#10020=CARTESIAN_POINT('',(28.7,25.9999999999999,-1.92966607280848));
#10021=CARTESIAN_POINT('',(29.,25.9999999999999,-1.92966607280848));
#10022=CARTESIAN_POINT('',(28.7,21.9999999999999,2.07033392719152));
#10023=CARTESIAN_POINT('Origin',(28.7,21.9999999999999,-1.92966607280848));
#10024=CARTESIAN_POINT('Origin',(28.7,21.9999999999999,-1.92966607280848));
#10025=CARTESIAN_POINT('Origin',(13.3,21.9999999999999,-1.92966607280848));
#10026=CARTESIAN_POINT('',(13.3,21.9999999999999,3.07033392719152));
#10027=CARTESIAN_POINT('Origin',(13.3,21.9999999999999,2.77033392719152));
#10028=CARTESIAN_POINT('',(13.3,26.9999999999999,-1.92966607280848));
#10029=CARTESIAN_POINT('Origin',(13.3,21.9999999999999,-1.92966607280848));
#10030=CARTESIAN_POINT('Origin',(13.3,21.9999999999999,-1.92966607280848));
#10031=CARTESIAN_POINT('Origin',(29.,21.9999999999999,-1.92966607280848));
#10032=CARTESIAN_POINT('',(28.7,26.9999999999999,-1.92966607280848));
#10033=CARTESIAN_POINT('',(29.,26.9999999999999,-1.92966607280848));
#10034=CARTESIAN_POINT('',(28.7,21.9999999999999,-6.92966607280848));
#10035=CARTESIAN_POINT('Origin',(28.7,21.9999999999999,-1.92966607280848));
#10036=CARTESIAN_POINT('Origin',(28.7,21.9999999999999,-1.92966607280848));
#10037=CARTESIAN_POINT('Origin',(28.7,21.9999999999999,-1.92966607280848));
#10038=CARTESIAN_POINT('',(29.,21.9999999999999,2.37033392719152));
#10039=CARTESIAN_POINT('Origin',(29.,21.9999999999999,-1.92966607280848));
#10040=CARTESIAN_POINT('Origin',(28.7,21.9999999999999,2.37033392719152));
#10041=CARTESIAN_POINT('Origin',(29.,21.9999999999999,-1.92966607280848));
#10042=CARTESIAN_POINT('',(29.,21.9999999999999,-6.62966607280848));
#10043=CARTESIAN_POINT('Origin',(29.,21.9999999999999,-1.92966607280848));
#10044=CARTESIAN_POINT('Origin',(28.7,21.9999999999999,-1.92966607280848));
#10045=CARTESIAN_POINT('Origin',(28.7,21.9999999999999,-6.62966607280848));
#10622=UNCERTAINTY_MEASURE_WITH_UNIT(LENGTH_MEASURE(0.01),#10640,
'DISTANCE_ACCURACY_VALUE',
'Maximum model space distance between geometric entities at asserted c
onnectivities');
#10627=UNCERTAINTY_MEASURE_WITH_UNIT(LENGTH_MEASURE(0.01),#10640,
'DISTANCE_ACCURACY_VALUE',
'Maximum model space distance between geometric entities at asserted c
onnectivities');
#10634=(
GEOMETRIC_REPRESENTATION_CONTEXT(3)
GLOBAL_UNCERTAINTY_ASSIGNED_CONTEXT((#10622))
GLOBAL_UNIT_ASSIGNED_CONTEXT((#10640,#10642,#10643))
REPRESENTATION_CONTEXT('','3D')
);
#10639=(
GEOMETRIC_REPRESENTATION_CONTEXT(3)
GLOBAL_UNCERTAINTY_ASSIGNED_CONTEXT((#10627))
GLOBAL_UNIT_ASSIGNED_CONTEXT((#10640,#10642,#10643))
REPRESENTATION_CONTEXT('','3D')
);
#10640=(
LENGTH_UNIT()
NAMED_UNIT(*)
SI_UNIT(.MILLI.,.METRE.)
);
#10642=(
NAMED_UNIT(*)
PLANE_ANGLE_UNIT()
SI_UNIT($,.RADIAN.)
);
#10643=(
NAMED_UNIT(*)
SI_UNIT($,.STERADIAN.)
SOLID_ANGLE_UNIT()
);
#10650=SHAPE_DEFINITION_REPRESENTATION(#10661,#10682);
#10661=PRODUCT_DEFINITION_SHAPE('',$,#10694);
#10682=SHAPE_REPRESENTATION('',(#6427),#10634);
#10687=PRODUCT_DEFINITION_CONTEXT('part definition',#10722,'design');
#10694=PRODUCT_DEFINITION('Bearing_02','Bearing_02',#10705,#10687);
#10705=PRODUCT_DEFINITION_FORMATION('',$,#10730);
#10722=APPLICATION_CONTEXT(
'Core Data for Automotive Mechanical Design Process');
#10723=PRODUCT_CONTEXT('part definition',#10722,'mechanical');
#10730=PRODUCT('Bearing_02','Bearing_02',$,(#10723));
#10784=COLOUR_RGB('Grey',0.48,0.52,0.57);
#10785=FILL_AREA_STYLE_COLOUR('',#10784);
#10786=FILL_AREA_STYLE('',(#10785));
#10787=SURFACE_STYLE_FILL_AREA(#10786);
#10788=SURFACE_SIDE_STYLE('',(#10787));
#10789=SURFACE_STYLE_USAGE(.BOTH.,#10788);
#10790=PRESENTATION_STYLE_ASSIGNMENT((#10789));
ENDSEC;
END-ISO-10303-21;
